ISO-10303-21;
HEADER;
/* Generated by software containing ST-Developer
 * from STEP Tools, Inc. (www.steptools.com) 
 */

FILE_DESCRIPTION(
/* description */ ('PAT-091'),
/* implementation_level */ '2;1');

FILE_NAME(
/* name */ 'Axle distance sleeve 5 mm (8).step',
/* time_stamp */ '2026-10-27T15:34:44-07:00',
/* author */ (''),
/* organization */ (''),
/* preprocessor_version */ 'ST-DEVELOPER v20.2',
/* originating_system */ 'Autodesk Translation Framework v15.17.0.0',
/* authorisation */ '');

FILE_SCHEMA (('AUTOMOTIVE_DESIGN { 1 0 10303 214 3 1 1 }'));
ENDSEC;

DATA;
#10=MECHANICAL_DESIGN_GEOMETRIC_PRESENTATION_REPRESENTATION('',(#1023),#25100);
#803=SHAPE_REPRESENTATION_RELATIONSHIP('SRR','None',#25567,#913);
#913=ADVANCED_BREP_SHAPE_REPRESENTATION('',(#1145),#25037);
#1023=STYLED_ITEM('',(#26191),#1145);
#1145=MANIFOLD_SOLID_BREP('Body1',#13302);
#1470=FACE_BOUND('',#3547,.T.);
#1471=FACE_BOUND('',#3549,.T.);
#1867=PLANE('',#15416);
#1868=PLANE('',#15417);
#2471=FACE_OUTER_BOUND('',#3544,.T.);
#2472=FACE_OUTER_BOUND('',#3545,.T.);
#2473=FACE_OUTER_BOUND('',#3546,.T.);
#2474=FACE_OUTER_BOUND('',#3548,.T.);
#3544=EDGE_LOOP('',(#10620,#10621,#10622,#10623));
#3545=EDGE_LOOP('',(#10624,#10625,#10626,#10627));
#3546=EDGE_LOOP('',(#10628));
#3547=EDGE_LOOP('',(#10629));
#3548=EDGE_LOOP('',(#10630));
#3549=EDGE_LOOP('',(#10631));
#4585=LINE('',#22867,#5325);
#4586=LINE('',#22873,#5326);
#5325=VECTOR('',#18583,0.604999999999997);
#5326=VECTOR('',#18590,0.799999999999997);
#5963=CIRCLE('',#15411,0.604999999999997);
#5964=CIRCLE('',#15412,0.604999999999997);
#5965=CIRCLE('',#15414,0.799999999999997);
#5966=CIRCLE('',#15415,0.799999999999997);
#6930=VERTEX_POINT('',#22864);
#6931=VERTEX_POINT('',#22866);
#6932=VERTEX_POINT('',#22870);
#6933=VERTEX_POINT('',#22872);
#8245=EDGE_CURVE('',#6930,#6930,#5963,.T.);
#8246=EDGE_CURVE('',#6930,#6931,#4585,.T.);
#8247=EDGE_CURVE('',#6931,#6931,#5964,.T.);
#8248=EDGE_CURVE('',#6932,#6932,#5965,.T.);
#8249=EDGE_CURVE('',#6932,#6933,#4586,.T.);
#8250=EDGE_CURVE('',#6933,#6933,#5966,.T.);
#10620=ORIENTED_EDGE('',*,*,#8245,.F.);
#10621=ORIENTED_EDGE('',*,*,#8246,.T.);
#10622=ORIENTED_EDGE('',*,*,#8247,.T.);
#10623=ORIENTED_EDGE('',*,*,#8246,.F.);
#10624=ORIENTED_EDGE('',*,*,#8248,.F.);
#10625=ORIENTED_EDGE('',*,*,#8249,.T.);
#10626=ORIENTED_EDGE('',*,*,#8250,.T.);
#10627=ORIENTED_EDGE('',*,*,#8249,.F.);
#10628=ORIENTED_EDGE('',*,*,#8248,.T.);
#10629=ORIENTED_EDGE('',*,*,#8245,.T.);
#10630=ORIENTED_EDGE('',*,*,#8250,.F.);
#10631=ORIENTED_EDGE('',*,*,#8247,.F.);
#12248=CYLINDRICAL_SURFACE('',#15410,0.604999999999997);
#12249=CYLINDRICAL_SURFACE('',#15413,0.799999999999997);
#12838=ADVANCED_FACE('',(#2471),#12248,.F.);
#12839=ADVANCED_FACE('',(#2472),#12249,.T.);
#12840=ADVANCED_FACE('',(#2473,#1470),#1867,.T.);
#12841=ADVANCED_FACE('',(#2474,#1471),#1868,.F.);
#13302=CLOSED_SHELL('',(#12838,#12839,#12840,#12841));
#15409=AXIS2_PLACEMENT_3D('',#22862,#18577,#18578);
#15410=AXIS2_PLACEMENT_3D('',#22863,#18579,#18580);
#15411=AXIS2_PLACEMENT_3D('',#22865,#18581,#18582);
#15412=AXIS2_PLACEMENT_3D('',#22868,#18584,#18585);
#15413=AXIS2_PLACEMENT_3D('',#22869,#18586,#18587);
#15414=AXIS2_PLACEMENT_3D('',#22871,#18588,#18589);
#15415=AXIS2_PLACEMENT_3D('',#22874,#18591,#18592);
#15416=AXIS2_PLACEMENT_3D('',#22875,#18593,#18594);
#15417=AXIS2_PLACEMENT_3D('',#22876,#18595,#18596);
#18577=DIRECTION('axis',(0.,0.,1.));
#18578=DIRECTION('refdir',(1.,0.,0.));
#18579=DIRECTION('center_axis',(0.,1.,0.));
#18580=DIRECTION('ref_axis',(1.,0.,0.));
#18581=DIRECTION('center_axis',(0.,-1.,0.));
#18582=DIRECTION('ref_axis',(1.,0.,0.));
#18583=DIRECTION('',(0.,-1.,0.));
#18584=DIRECTION('center_axis',(0.,-1.,0.));
#18585=DIRECTION('ref_axis',(1.,0.,0.));
#18586=DIRECTION('center_axis',(0.,1.,0.));
#18587=DIRECTION('ref_axis',(1.,0.,0.));
#18588=DIRECTION('center_axis',(0.,1.,0.));
#18589=DIRECTION('ref_axis',(1.,0.,0.));
#18590=DIRECTION('',(0.,-1.,0.));
#18591=DIRECTION('center_axis',(0.,1.,0.));
#18592=DIRECTION('ref_axis',(1.,0.,0.));
#18593=DIRECTION('center_axis',(0.,1.,0.));
#18594=DIRECTION('ref_axis',(1.,0.,0.));
#18595=DIRECTION('center_axis',(0.,1.,0.));
#18596=DIRECTION('ref_axis',(1.,0.,0.));
#22862=CARTESIAN_POINT('',(0.,0.,0.));
#22863=CARTESIAN_POINT('Origin',(38.7298334620742,6.,13.));
#22864=CARTESIAN_POINT('',(38.1248334620742,6.5,13.));
#22865=CARTESIAN_POINT('Origin',(38.7298334620742,6.5,13.));
#22866=CARTESIAN_POINT('',(38.1248334620742,6.,13.));
#22867=CARTESIAN_POINT('',(38.1248334620742,6.,13.));
#22868=CARTESIAN_POINT('Origin',(38.7298334620742,6.,13.));
#22869=CARTESIAN_POINT('Origin',(38.7298334620742,6.,13.));
#22870=CARTESIAN_POINT('',(37.9298334620742,6.5,13.));
#22871=CARTESIAN_POINT('Origin',(38.7298334620742,6.5,13.));
#22872=CARTESIAN_POINT('',(37.9298334620742,6.,13.));
#22873=CARTESIAN_POINT('',(37.9298334620742,6.,13.));
#22874=CARTESIAN_POINT('Origin',(38.7298334620742,6.,13.));
#22875=CARTESIAN_POINT('Origin',(38.7298334620742,6.5,13.));
#22876=CARTESIAN_POINT('Origin',(38.7298334620742,6.,13.));
#24916=UNCERTAINTY_MEASURE_WITH_UNIT(LENGTH_MEASURE(0.001),#25101,
'DISTANCE_ACCURACY_VALUE',
'Maximum model space distance between geometric entities at asserted c
onnectivities');
#24979=UNCERTAINTY_MEASURE_WITH_UNIT(LENGTH_MEASURE(0.001),#25101,
'DISTANCE_ACCURACY_VALUE',
'Maximum model space distance between geometric entities at asserted c
onnectivities');
#25037=(
GEOMETRIC_REPRESENTATION_CONTEXT(3)
GLOBAL_UNCERTAINTY_ASSIGNED_CONTEXT((#24916))
GLOBAL_UNIT_ASSIGNED_CONTEXT((#25101,#25103,#25104))
REPRESENTATION_CONTEXT('','3D')
);
#25100=(
GEOMETRIC_REPRESENTATION_CONTEXT(3)
GLOBAL_UNCERTAINTY_ASSIGNED_CONTEXT((#24979))
GLOBAL_UNIT_ASSIGNED_CONTEXT((#25101,#25103,#25104))
REPRESENTATION_CONTEXT('','3D')
);
#25101=(
LENGTH_UNIT()
NAMED_UNIT(*)
SI_UNIT(.CENTI.,.METRE.)
);
#25103=(
NAMED_UNIT(*)
PLANE_ANGLE_UNIT()
SI_UNIT($,.RADIAN.)
);
#25104=(
NAMED_UNIT(*)
SI_UNIT($,.STERADIAN.)
SOLID_ANGLE_UNIT()
);
#25162=SHAPE_DEFINITION_REPRESENTATION(#25282,#25567);
#25282=PRODUCT_DEFINITION_SHAPE('',$,#25688);
#25567=SHAPE_REPRESENTATION('',(#15409),#25037);
#25630=PRODUCT_DEFINITION_CONTEXT('part definition',#25992,'design');
#25688=PRODUCT_DEFINITION('Axle distance sleeve 5 mm (8)',
'Axle distance sleeve 5 mm (8)',#25808,#25630);
#25808=PRODUCT_DEFINITION_FORMATION('',$,#26051);
#25992=APPLICATION_CONTEXT(
'Core Data for Automotive Mechanical Design Process');
#25993=PRODUCT_CONTEXT('part definition',#25992,'mechanical');
#26051=PRODUCT('Axle distance sleeve 5 mm (8)',
'Axle distance sleeve 5 mm (8)','Axle distance sleeve 5 mm (8)',(#25993));
#26185=COLOUR_RGB('Grey',0.48,0.52,0.57);
#26186=FILL_AREA_STYLE_COLOUR('',#26185);
#26187=FILL_AREA_STYLE('',(#26186));
#26188=SURFACE_STYLE_FILL_AREA(#26187);
#26189=SURFACE_SIDE_STYLE('',(#26188));
#26190=SURFACE_STYLE_USAGE(.BOTH.,#26189);
#26191=PRESENTATION_STYLE_ASSIGNMENT((#26190));
ENDSEC;
END-ISO-10303-21;
